ISO-10303-21;
HEADER;
/* Generated by software containing ST-Developer
 * from STEP Tools, Inc. (www.steptools.com) 
 */

FILE_DESCRIPTION(
/* description */ ('XY cross-slide table'),
/* implementation_level */ '2;1');

FILE_NAME(
/* name */ 'M5x14 Cap Screw.step',
/* time_stamp */ '2026-10-28T03:22:46-07:00',
/* author */ (''),
/* organization */ (''),
/* preprocessor_version */ 'ST-DEVELOPER v20.2',
/* originating_system */ 'Autodesk Translation Framework v15.17.0.0',
/* authorisation */ '');

FILE_SCHEMA (('AUTOMOTIVE_DESIGN { 1 0 10303 214 3 1 1 }'));
ENDSEC;

DATA;
#10=MECHANICAL_DESIGN_GEOMETRIC_PRESENTATION_REPRESENTATION('',(#1761),#62984);
#23=ORIENTED_CLOSED_SHELL('',*,#23059,.F.);
#32=BREP_WITH_VOIDS('Body1',#23060,(#23));
#1475=CONICAL_SURFACE('',#25805,0.4,0.785398163397448);
#1476=CONICAL_SURFACE('',#25809,0.41,0.785398163397448);
#1477=CONICAL_SURFACE('',#25813,0.26,0.463647609000806);
#1565=SHAPE_REPRESENTATION_RELATIONSHIP('SRR','None',#63422,#1648);
#1648=ADVANCED_BREP_SHAPE_REPRESENTATION('',(#32),#62959);
#1761=STYLED_ITEM('',(#63919),#32);
#2219=FACE_BOUND('',#5434,.T.);
#2695=PLANE('',#25793);
#2696=PLANE('',#25794);
#2697=PLANE('',#25795);
#2698=PLANE('',#25796);
#2699=PLANE('',#25797);
#2700=PLANE('',#25798);
#2701=PLANE('',#25799);
#2702=PLANE('',#25800);
#2703=PLANE('',#25801);
#2704=PLANE('',#25803);
#2705=PLANE('',#25811);
#3774=FACE_OUTER_BOUND('',#5420,.T.);
#3775=FACE_OUTER_BOUND('',#5421,.T.);
#3776=FACE_OUTER_BOUND('',#5422,.T.);
#3777=FACE_OUTER_BOUND('',#5423,.T.);
#3778=FACE_OUTER_BOUND('',#5424,.T.);
#3779=FACE_OUTER_BOUND('',#5425,.T.);
#3780=FACE_OUTER_BOUND('',#5426,.T.);
#3781=FACE_OUTER_BOUND('',#5427,.T.);
#3782=FACE_OUTER_BOUND('',#5428,.T.);
#3783=FACE_OUTER_BOUND('',#5429,.T.);
#3784=FACE_OUTER_BOUND('',#5430,.T.);
#3785=FACE_OUTER_BOUND('',#5431,.T.);
#3786=FACE_OUTER_BOUND('',#5432,.T.);
#3787=FACE_OUTER_BOUND('',#5433,.T.);
#3788=FACE_OUTER_BOUND('',#5435,.T.);
#3789=FACE_OUTER_BOUND('',#5436,.T.);
#5420=EDGE_LOOP('',(#19038,#19039,#19040,#19041));
#5421=EDGE_LOOP('',(#19042,#19043,#19044,#19045));
#5422=EDGE_LOOP('',(#19046,#19047,#19048,#19049));
#5423=EDGE_LOOP('',(#19050,#19051,#19052,#19053));
#5424=EDGE_LOOP('',(#19054,#19055,#19056,#19057));
#5425=EDGE_LOOP('',(#19058,#19059,#19060,#19061));
#5426=EDGE_LOOP('',(#19062,#19063,#19064,#19065,#19066,#19067));
#5427=EDGE_LOOP('',(#19068,#19069,#19070,#19071,#19072,#19073));
#5428=EDGE_LOOP('',(#19074));
#5429=EDGE_LOOP('',(#19075));
#5430=EDGE_LOOP('',(#19076,#19077,#19078,#19079));
#5431=EDGE_LOOP('',(#19080,#19081,#19082,#19083));
#5432=EDGE_LOOP('',(#19084,#19085,#19086,#19087));
#5433=EDGE_LOOP('',(#19088));
#5434=EDGE_LOOP('',(#19089));
#5435=EDGE_LOOP('',(#19090,#19091,#19092,#19093));
#5436=EDGE_LOOP('',(#19094,#19095,#19096,#19097));
#6869=LINE('',#49648,#8356);
#6870=LINE('',#49650,#8357);
#6871=LINE('',#49652,#8358);
#6872=LINE('',#49653,#8359);
#6873=LINE('',#49656,#8360);
#6874=LINE('',#49658,#8361);
#6875=LINE('',#49659,#8362);
#6876=LINE('',#49662,#8363);
#6877=LINE('',#49664,#8364);
#6878=LINE('',#49665,#8365);
#6879=LINE('',#49668,#8366);
#6880=LINE('',#49670,#8367);
#6881=LINE('',#49671,#8368);
#6882=LINE('',#49674,#8369);
#6883=LINE('',#49676,#8370);
#6884=LINE('',#49677,#8371);
#6885=LINE('',#49679,#8372);
#6886=LINE('',#49680,#8373);
#6887=LINE('',#49692,#8374);
#6888=LINE('',#49696,#8375);
#6889=LINE('',#49700,#8376);
#6890=LINE('',#49707,#8377);
#6891=LINE('',#49709,#8378);
#8356=VECTOR('',#31012,1.);
#8357=VECTOR('',#31013,1.);
#8358=VECTOR('',#31014,1.);
#8359=VECTOR('',#31015,1.);
#8360=VECTOR('',#31018,1.);
#8361=VECTOR('',#31019,1.);
#8362=VECTOR('',#31020,1.);
#8363=VECTOR('',#31023,1.);
#8364=VECTOR('',#31024,1.);
#8365=VECTOR('',#31025,1.);
#8366=VECTOR('',#31028,1.);
#8367=VECTOR('',#31029,1.);
#8368=VECTOR('',#31030,1.);
#8369=VECTOR('',#31033,1.);
#8370=VECTOR('',#31034,1.);
#8371=VECTOR('',#31035,1.);
#8372=VECTOR('',#31038,1.);
#8373=VECTOR('',#31039,1.);
#8374=VECTOR('',#31056,0.4);
#8375=VECTOR('',#31061,0.425);
#8376=VECTOR('',#31066,0.41);
#8377=VECTOR('',#31075,0.26);
#8378=VECTOR('',#31078,0.25);
#9608=CIRCLE('',#25802,0.24505);
#9609=CIRCLE('',#25804,0.375);
#9610=CIRCLE('',#25806,0.425);
#9611=CIRCLE('',#25808,0.425);
#9612=CIRCLE('',#25810,0.395);
#9613=CIRCLE('',#25812,0.27);
#9614=CIRCLE('',#25814,0.24505);
#11175=VERTEX_POINT('',#49646);
#11176=VERTEX_POINT('',#49647);
#11177=VERTEX_POINT('',#49649);
#11178=VERTEX_POINT('',#49651);
#11179=VERTEX_POINT('',#49655);
#11180=VERTEX_POINT('',#49657);
#11181=VERTEX_POINT('',#49661);
#11182=VERTEX_POINT('',#49663);
#11183=VERTEX_POINT('',#49667);
#11184=VERTEX_POINT('',#49669);
#11185=VERTEX_POINT('',#49673);
#11186=VERTEX_POINT('',#49675);
#11187=VERTEX_POINT('',#49684);
#11188=VERTEX_POINT('',#49687);
#11189=VERTEX_POINT('',#49690);
#11190=VERTEX_POINT('',#49694);
#11191=VERTEX_POINT('',#49698);
#11192=VERTEX_POINT('',#49702);
#11193=VERTEX_POINT('',#49705);
#13903=EDGE_CURVE('',#11175,#11176,#6869,.T.);
#13904=EDGE_CURVE('',#11176,#11177,#6870,.T.);
#13905=EDGE_CURVE('',#11177,#11178,#6871,.T.);
#13906=EDGE_CURVE('',#11175,#11178,#6872,.T.);
#13907=EDGE_CURVE('',#11176,#11179,#6873,.T.);
#13908=EDGE_CURVE('',#11179,#11180,#6874,.T.);
#13909=EDGE_CURVE('',#11180,#11177,#6875,.T.);
#13910=EDGE_CURVE('',#11179,#11181,#6876,.T.);
#13911=EDGE_CURVE('',#11181,#11182,#6877,.T.);
#13912=EDGE_CURVE('',#11182,#11180,#6878,.T.);
#13913=EDGE_CURVE('',#11181,#11183,#6879,.T.);
#13914=EDGE_CURVE('',#11183,#11184,#6880,.T.);
#13915=EDGE_CURVE('',#11184,#11182,#6881,.T.);
#13916=EDGE_CURVE('',#11183,#11185,#6882,.T.);
#13917=EDGE_CURVE('',#11185,#11186,#6883,.T.);
#13918=EDGE_CURVE('',#11186,#11184,#6884,.T.);
#13919=EDGE_CURVE('',#11185,#11175,#6885,.T.);
#13920=EDGE_CURVE('',#11178,#11186,#6886,.T.);
#13921=EDGE_CURVE('',#11187,#11187,#9608,.T.);
#13922=EDGE_CURVE('',#11188,#11188,#9609,.T.);
#13923=EDGE_CURVE('',#11189,#11189,#9610,.T.);
#13924=EDGE_CURVE('',#11189,#11188,#6887,.T.);
#13925=EDGE_CURVE('',#11190,#11190,#9611,.T.);
#13926=EDGE_CURVE('',#11190,#11189,#6888,.T.);
#13927=EDGE_CURVE('',#11191,#11191,#9612,.T.);
#13928=EDGE_CURVE('',#11191,#11190,#6889,.T.);
#13929=EDGE_CURVE('',#11192,#11192,#9613,.T.);
#13930=EDGE_CURVE('',#11193,#11193,#9614,.F.);
#13931=EDGE_CURVE('',#11193,#11192,#6890,.T.);
#13932=EDGE_CURVE('',#11187,#11193,#6891,.T.);
#19038=ORIENTED_EDGE('',*,*,#13903,.T.);
#19039=ORIENTED_EDGE('',*,*,#13904,.T.);
#19040=ORIENTED_EDGE('',*,*,#13905,.T.);
#19041=ORIENTED_EDGE('',*,*,#13906,.F.);
#19042=ORIENTED_EDGE('',*,*,#13907,.T.);
#19043=ORIENTED_EDGE('',*,*,#13908,.T.);
#19044=ORIENTED_EDGE('',*,*,#13909,.T.);
#19045=ORIENTED_EDGE('',*,*,#13904,.F.);
#19046=ORIENTED_EDGE('',*,*,#13910,.T.);
#19047=ORIENTED_EDGE('',*,*,#13911,.T.);
#19048=ORIENTED_EDGE('',*,*,#13912,.T.);
#19049=ORIENTED_EDGE('',*,*,#13908,.F.);
#19050=ORIENTED_EDGE('',*,*,#13913,.T.);
#19051=ORIENTED_EDGE('',*,*,#13914,.T.);
#19052=ORIENTED_EDGE('',*,*,#13915,.T.);
#19053=ORIENTED_EDGE('',*,*,#13911,.F.);
#19054=ORIENTED_EDGE('',*,*,#13916,.T.);
#19055=ORIENTED_EDGE('',*,*,#13917,.T.);
#19056=ORIENTED_EDGE('',*,*,#13918,.T.);
#19057=ORIENTED_EDGE('',*,*,#13914,.F.);
#19058=ORIENTED_EDGE('',*,*,#13919,.T.);
#19059=ORIENTED_EDGE('',*,*,#13906,.T.);
#19060=ORIENTED_EDGE('',*,*,#13920,.T.);
#19061=ORIENTED_EDGE('',*,*,#13917,.F.);
#19062=ORIENTED_EDGE('',*,*,#13919,.F.);
#19063=ORIENTED_EDGE('',*,*,#13916,.F.);
#19064=ORIENTED_EDGE('',*,*,#13913,.F.);
#19065=ORIENTED_EDGE('',*,*,#13910,.F.);
#19066=ORIENTED_EDGE('',*,*,#13907,.F.);
#19067=ORIENTED_EDGE('',*,*,#13903,.F.);
#19068=ORIENTED_EDGE('',*,*,#13920,.F.);
#19069=ORIENTED_EDGE('',*,*,#13905,.F.);
#19070=ORIENTED_EDGE('',*,*,#13909,.F.);
#19071=ORIENTED_EDGE('',*,*,#13912,.F.);
#19072=ORIENTED_EDGE('',*,*,#13915,.F.);
#19073=ORIENTED_EDGE('',*,*,#13918,.F.);
#19074=ORIENTED_EDGE('',*,*,#13921,.F.);
#19075=ORIENTED_EDGE('',*,*,#13922,.F.);
#19076=ORIENTED_EDGE('',*,*,#13923,.F.);
#19077=ORIENTED_EDGE('',*,*,#13924,.T.);
#19078=ORIENTED_EDGE('',*,*,#13922,.T.);
#19079=ORIENTED_EDGE('',*,*,#13924,.F.);
#19080=ORIENTED_EDGE('',*,*,#13925,.F.);
#19081=ORIENTED_EDGE('',*,*,#13926,.T.);
#19082=ORIENTED_EDGE('',*,*,#13923,.T.);
#19083=ORIENTED_EDGE('',*,*,#13926,.F.);
#19084=ORIENTED_EDGE('',*,*,#13927,.F.);
#19085=ORIENTED_EDGE('',*,*,#13928,.T.);
#19086=ORIENTED_EDGE('',*,*,#13925,.T.);
#19087=ORIENTED_EDGE('',*,*,#13928,.F.);
#19088=ORIENTED_EDGE('',*,*,#13927,.T.);
#19089=ORIENTED_EDGE('',*,*,#13929,.F.);
#19090=ORIENTED_EDGE('',*,*,#13930,.F.);
#19091=ORIENTED_EDGE('',*,*,#13931,.T.);
#19092=ORIENTED_EDGE('',*,*,#13929,.T.);
#19093=ORIENTED_EDGE('',*,*,#13931,.F.);
#19094=ORIENTED_EDGE('',*,*,#13921,.T.);
#19095=ORIENTED_EDGE('',*,*,#13932,.T.);
#19096=ORIENTED_EDGE('',*,*,#13930,.T.);
#19097=ORIENTED_EDGE('',*,*,#13932,.F.);
#21440=CYLINDRICAL_SURFACE('',#25807,0.425);
#21441=CYLINDRICAL_SURFACE('',#25815,0.24505);
#22555=ADVANCED_FACE('',(#3774),#2695,.F.);
#22556=ADVANCED_FACE('',(#3775),#2696,.F.);
#22557=ADVANCED_FACE('',(#3776),#2697,.F.);
#22558=ADVANCED_FACE('',(#3777),#2698,.F.);
#22559=ADVANCED_FACE('',(#3778),#2699,.F.);
#22560=ADVANCED_FACE('',(#3779),#2700,.F.);
#22561=ADVANCED_FACE('',(#3780),#2701,.F.);
#22562=ADVANCED_FACE('',(#3781),#2702,.F.);
#22563=ADVANCED_FACE('',(#3782),#2703,.F.);
#22564=ADVANCED_FACE('',(#3783),#2704,.T.);
#22565=ADVANCED_FACE('',(#3784),#1475,.T.);
#22566=ADVANCED_FACE('',(#3785),#21440,.T.);
#22567=ADVANCED_FACE('',(#3786),#1476,.T.);
#22568=ADVANCED_FACE('',(#3787,#2219),#2705,.T.);
#22569=ADVANCED_FACE('',(#3788),#1477,.T.);
#22570=ADVANCED_FACE('',(#3789),#21441,.T.);
#23059=CLOSED_SHELL('',(#22555,#22556,#22557,#22558,#22559,#22560,#22561,
#22562));
#23060=CLOSED_SHELL('',(#22563,#22564,#22565,#22566,#22567,#22568,#22569,
#22570));
#25792=AXIS2_PLACEMENT_3D('',#49644,#31008,#31009);
#25793=AXIS2_PLACEMENT_3D('',#49645,#31010,#31011);
#25794=AXIS2_PLACEMENT_3D('',#49654,#31016,#31017);
#25795=AXIS2_PLACEMENT_3D('',#49660,#31021,#31022);
#25796=AXIS2_PLACEMENT_3D('',#49666,#31026,#31027);
#25797=AXIS2_PLACEMENT_3D('',#49672,#31031,#31032);
#25798=AXIS2_PLACEMENT_3D('',#49678,#31036,#31037);
#25799=AXIS2_PLACEMENT_3D('',#49681,#31040,#31041);
#25800=AXIS2_PLACEMENT_3D('',#49682,#31042,#31043);
#25801=AXIS2_PLACEMENT_3D('',#49683,#31044,#31045);
#25802=AXIS2_PLACEMENT_3D('',#49685,#31046,#31047);
#25803=AXIS2_PLACEMENT_3D('',#49686,#31048,#31049);
#25804=AXIS2_PLACEMENT_3D('',#49688,#31050,#31051);
#25805=AXIS2_PLACEMENT_3D('',#49689,#31052,#31053);
#25806=AXIS2_PLACEMENT_3D('',#49691,#31054,#31055);
#25807=AXIS2_PLACEMENT_3D('',#49693,#31057,#31058);
#25808=AXIS2_PLACEMENT_3D('',#49695,#31059,#31060);
#25809=AXIS2_PLACEMENT_3D('',#49697,#31062,#31063);
#25810=AXIS2_PLACEMENT_3D('',#49699,#31064,#31065);
#25811=AXIS2_PLACEMENT_3D('',#49701,#31067,#31068);
#25812=AXIS2_PLACEMENT_3D('',#49703,#31069,#31070);
#25813=AXIS2_PLACEMENT_3D('',#49704,#31071,#31072);
#25814=AXIS2_PLACEMENT_3D('',#49706,#31073,#31074);
#25815=AXIS2_PLACEMENT_3D('',#49708,#31076,#31077);
#31008=DIRECTION('axis',(0.,0.,1.));
#31009=DIRECTION('refdir',(1.,0.,0.));
#31010=DIRECTION('center_axis',(0.866025403784439,0.,-0.5));
#31011=DIRECTION('ref_axis',(0.5,0.,0.866025403784439));
#31012=DIRECTION('',(-0.5,0.,-0.866025403784439));
#31013=DIRECTION('',(0.,-1.,0.));
#31014=DIRECTION('',(0.5,0.,0.866025403784439));
#31015=DIRECTION('',(0.,-1.,0.));
#31016=DIRECTION('center_axis',(1.20185167898973E-16,0.,-1.));
#31017=DIRECTION('ref_axis',(1.,0.,1.20185167898973E-16));
#31018=DIRECTION('',(-1.,0.,-1.20185167898973E-16));
#31019=DIRECTION('',(0.,-1.,0.));
#31020=DIRECTION('',(1.,0.,1.20185167898973E-16));
#31021=DIRECTION('center_axis',(-0.866025403784439,0.,-0.5));
#31022=DIRECTION('ref_axis',(0.5,0.,-0.866025403784439));
#31023=DIRECTION('',(-0.5,0.,0.866025403784439));
#31024=DIRECTION('',(0.,-1.,0.));
#31025=DIRECTION('',(0.5,0.,-0.866025403784439));
#31026=DIRECTION('center_axis',(-0.866025403784439,0.,0.5));
#31027=DIRECTION('ref_axis',(-0.5,0.,-0.866025403784439));
#31028=DIRECTION('',(0.5,0.,0.866025403784439));
#31029=DIRECTION('',(0.,-1.,0.));
#31030=DIRECTION('',(-0.5,0.,-0.866025403784439));
#31031=DIRECTION('center_axis',(-2.40370335797945E-16,0.,1.));
#31032=DIRECTION('ref_axis',(-1.,0.,-2.40370335797945E-16));
#31033=DIRECTION('',(1.,0.,2.40370335797945E-16));
#31034=DIRECTION('',(0.,-1.,0.));
#31035=DIRECTION('',(-1.,0.,-2.40370335797945E-16));
#31036=DIRECTION('center_axis',(0.866025403784439,0.,0.5));
#31037=DIRECTION('ref_axis',(-0.5,0.,0.866025403784439));
#31038=DIRECTION('',(0.5,0.,-0.866025403784439));
#31039=DIRECTION('',(-0.5,0.,0.866025403784439));
#31040=DIRECTION('center_axis',(0.,1.,0.));
#31041=DIRECTION('ref_axis',(1.,0.,0.));
#31042=DIRECTION('center_axis',(0.,-1.,0.));
#31043=DIRECTION('ref_axis',(0.,0.,-1.));
#31044=DIRECTION('center_axis',(0.,1.,0.));
#31045=DIRECTION('ref_axis',(1.,0.,0.));
#31046=DIRECTION('center_axis',(0.,1.,0.));
#31047=DIRECTION('ref_axis',(1.,0.,0.));
#31048=DIRECTION('center_axis',(0.,1.,0.));
#31049=DIRECTION('ref_axis',(0.,0.,1.));
#31050=DIRECTION('center_axis',(0.,-1.,0.));
#31051=DIRECTION('ref_axis',(1.,0.,0.));
#31052=DIRECTION('center_axis',(0.,-1.,0.));
#31053=DIRECTION('ref_axis',(1.,0.,0.));
#31054=DIRECTION('center_axis',(0.,-1.,0.));
#31055=DIRECTION('ref_axis',(1.,0.,0.));
#31056=DIRECTION('',(0.707106781186548,0.707106781186547,8.65956056235493E-17));
#31057=DIRECTION('center_axis',(0.,-1.,0.));
#31058=DIRECTION('ref_axis',(1.,0.,0.));
#31059=DIRECTION('center_axis',(0.,-1.,0.));
#31060=DIRECTION('ref_axis',(1.,0.,0.));
#31061=DIRECTION('',(0.,1.,0.));
#31062=DIRECTION('center_axis',(0.,1.,0.));
#31063=DIRECTION('ref_axis',(1.,0.,0.));
#31064=DIRECTION('center_axis',(0.,-1.,0.));
#31065=DIRECTION('ref_axis',(1.,0.,0.));
#31066=DIRECTION('',(-0.707106781186547,0.707106781186548,-8.65956056235493E-17));
#31067=DIRECTION('center_axis',(0.,-1.,0.));
#31068=DIRECTION('ref_axis',(0.,0.,-1.));
#31069=DIRECTION('center_axis',(0.,-1.,0.));
#31070=DIRECTION('ref_axis',(1.,0.,0.));
#31071=DIRECTION('center_axis',(0.,1.,0.));
#31072=DIRECTION('ref_axis',(1.,0.,0.));
#31073=DIRECTION('center_axis',(0.,1.,0.));
#31074=DIRECTION('ref_axis',(1.,0.,0.));
#31075=DIRECTION('',(-0.447213595499958,0.894427190999916,-5.47678698264203E-17));
#31076=DIRECTION('center_axis',(0.,-1.,0.));
#31077=DIRECTION('ref_axis',(1.,0.,0.));
#31078=DIRECTION('',(0.,1.,0.));
#49644=CARTESIAN_POINT('',(0.,0.,0.));
#49645=CARTESIAN_POINT('Origin',(0.115470053837925,-0.5,-0.2));
#49646=CARTESIAN_POINT('',(0.23094010767585,-0.5,0.));
#49647=CARTESIAN_POINT('',(0.115470053837925,-0.5,-0.2));
#49648=CARTESIAN_POINT('',(0.23094010767585,-0.5,0.));
#49649=CARTESIAN_POINT('',(0.115470053837925,-0.8,-0.2));
#49650=CARTESIAN_POINT('',(0.115470053837925,-0.5,-0.2));
#49651=CARTESIAN_POINT('',(0.23094010767585,-0.8,0.));
#49652=CARTESIAN_POINT('',(0.23094010767585,-0.8,0.));
#49653=CARTESIAN_POINT('',(0.23094010767585,-0.5,0.));
#49654=CARTESIAN_POINT('Origin',(-0.115470053837925,-0.5,-0.2));
#49655=CARTESIAN_POINT('',(-0.115470053837925,-0.5,-0.2));
#49656=CARTESIAN_POINT('',(0.115470053837925,-0.5,-0.2));
#49657=CARTESIAN_POINT('',(-0.115470053837925,-0.8,-0.2));
#49658=CARTESIAN_POINT('',(-0.115470053837925,-0.5,-0.2));
#49659=CARTESIAN_POINT('',(0.115470053837925,-0.8,-0.2));
#49660=CARTESIAN_POINT('Origin',(-0.23094010767585,-0.5,-2.77555756156289E-17));
#49661=CARTESIAN_POINT('',(-0.23094010767585,-0.5,-2.82820063659975E-17));
#49662=CARTESIAN_POINT('',(-0.115470053837925,-0.5,-0.2));
#49663=CARTESIAN_POINT('',(-0.23094010767585,-0.8,-2.77555756156289E-17));
#49664=CARTESIAN_POINT('',(-0.23094010767585,-0.5,-2.82820063659975E-17));
#49665=CARTESIAN_POINT('',(-0.115470053837925,-0.8,-0.2));
#49666=CARTESIAN_POINT('Origin',(-0.115470053837925,-0.5,0.2));
#49667=CARTESIAN_POINT('',(-0.115470053837925,-0.5,0.2));
#49668=CARTESIAN_POINT('',(-0.23094010767585,-0.5,-2.82820063659975E-17));
#49669=CARTESIAN_POINT('',(-0.115470053837925,-0.8,0.2));
#49670=CARTESIAN_POINT('',(-0.115470053837925,-0.5,0.2));
#49671=CARTESIAN_POINT('',(-0.23094010767585,-0.8,-2.82820063659975E-17));
#49672=CARTESIAN_POINT('Origin',(0.115470053837925,-0.5,0.2));
#49673=CARTESIAN_POINT('',(0.115470053837925,-0.5,0.2));
#49674=CARTESIAN_POINT('',(-0.115470053837925,-0.5,0.2));
#49675=CARTESIAN_POINT('',(0.115470053837925,-0.8,0.2));
#49676=CARTESIAN_POINT('',(0.115470053837925,-0.5,0.2));
#49677=CARTESIAN_POINT('',(-0.115470053837925,-0.8,0.2));
#49678=CARTESIAN_POINT('Origin',(0.23094010767585,-0.5,0.));
#49679=CARTESIAN_POINT('',(0.115470053837925,-0.5,0.2));
#49680=CARTESIAN_POINT('',(0.115470053837925,-0.8,0.2));
#49681=CARTESIAN_POINT('Origin',(0.,-0.5,0.));
#49682=CARTESIAN_POINT('Origin',(0.,-0.8,0.));
#49683=CARTESIAN_POINT('Origin',(0.,-1.4,0.));
#49684=CARTESIAN_POINT('',(-0.24505,-1.4,3.00099698131059E-17));
#49685=CARTESIAN_POINT('Origin',(0.,-1.4,0.));
#49686=CARTESIAN_POINT('Origin',(0.375,0.5,0.));
#49687=CARTESIAN_POINT('',(-0.375,0.5,-4.59242549680257E-17));
#49688=CARTESIAN_POINT('Origin',(0.,0.5,0.));
#49689=CARTESIAN_POINT('Origin',(0.,0.475,0.));
#49690=CARTESIAN_POINT('',(-0.425,0.45,-5.20474889637625E-17));
#49691=CARTESIAN_POINT('Origin',(0.,0.45,0.));
#49692=CARTESIAN_POINT('',(-0.4,0.475,-4.89858719658941E-17));
#49693=CARTESIAN_POINT('Origin',(0.,0.24,0.));
#49694=CARTESIAN_POINT('',(-0.425,0.0299999999999998,-5.20474889637625E-17));
#49695=CARTESIAN_POINT('Origin',(0.,0.0299999999999998,0.));
#49696=CARTESIAN_POINT('',(-0.425,0.24,-5.20474889637625E-17));
#49697=CARTESIAN_POINT('Origin',(0.,0.0150000000000001,0.));
#49698=CARTESIAN_POINT('',(-0.395,4.85722573273506E-17,-4.83735485663204E-17));
#49699=CARTESIAN_POINT('Origin',(0.,0.,0.));
#49700=CARTESIAN_POINT('',(-0.41,0.0150000000000001,-5.02105187650415E-17));
#49701=CARTESIAN_POINT('Origin',(0.27,0.,0.));
#49702=CARTESIAN_POINT('',(-0.27,0.,-3.30654635769785E-17));
#49703=CARTESIAN_POINT('Origin',(0.,0.,0.));
#49704=CARTESIAN_POINT('Origin',(0.,-0.02,0.));
#49705=CARTESIAN_POINT('',(-0.24505,-0.0498999999999999,3.00099698131059E-17));
#49706=CARTESIAN_POINT('Origin',(0.,-0.0498999999999999,0.));
#49707=CARTESIAN_POINT('',(-0.26,-0.02,-3.18408167778312E-17));
#49708=CARTESIAN_POINT('Origin',(0.,-0.995,0.));
#49709=CARTESIAN_POINT('',(-0.24505,-0.995,-3.00099698131059E-17));
#62860=UNCERTAINTY_MEASURE_WITH_UNIT(LENGTH_MEASURE(0.001),#62985,
'DISTANCE_ACCURACY_VALUE',
'Maximum model space distance between geometric entities at asserted c
onnectivities');
#62885=UNCERTAINTY_MEASURE_WITH_UNIT(LENGTH_MEASURE(0.001),#62985,
'DISTANCE_ACCURACY_VALUE',
'Maximum model space distance between geometric entities at asserted c
onnectivities');
#62959=(
GEOMETRIC_REPRESENTATION_CONTEXT(3)
GLOBAL_UNCERTAINTY_ASSIGNED_CONTEXT((#62860))
GLOBAL_UNIT_ASSIGNED_CONTEXT((#62985,#62987,#62988))
REPRESENTATION_CONTEXT('','3D')
);
#62984=(
GEOMETRIC_REPRESENTATION_CONTEXT(3)
GLOBAL_UNCERTAINTY_ASSIGNED_CONTEXT((#62885))
GLOBAL_UNIT_ASSIGNED_CONTEXT((#62985,#62987,#62988))
REPRESENTATION_CONTEXT('','3D')
);
#62985=(
LENGTH_UNIT()
NAMED_UNIT(*)
SI_UNIT(.CENTI.,.METRE.)
);
#62987=(
NAMED_UNIT(*)
PLANE_ANGLE_UNIT()
SI_UNIT($,.RADIAN.)
);
#62988=(
NAMED_UNIT(*)
SI_UNIT($,.STERADIAN.)
SOLID_ANGLE_UNIT()
);
#63062=SHAPE_DEFINITION_REPRESENTATION(#63250,#63422);
#63250=PRODUCT_DEFINITION_SHAPE('',$,#63521);
#63422=SHAPE_REPRESENTATION('',(#25792),#62959);
#63447=PRODUCT_DEFINITION_CONTEXT('part definition',#63743,'design');
#63521=PRODUCT_DEFINITION('M5x14 Cap Screw','M5x14 Cap Screw',#63619,#63447);
#63619=PRODUCT_DEFINITION_FORMATION('',$,#63818);
#63743=APPLICATION_CONTEXT(
'Core Data for Automotive Mechanical Design Process');
#63744=PRODUCT_CONTEXT('part definition',#63743,'mechanical');
#63818=PRODUCT('M5x14 Cap Screw','M5x14 Cap Screw','M5x14 Cap Screw',(#63744));
#63913=COLOUR_RGB('Black',0.12,0.14,0.17);
#63914=FILL_AREA_STYLE_COLOUR('',#63913);
#63915=FILL_AREA_STYLE('',(#63914));
#63916=SURFACE_STYLE_FILL_AREA(#63915);
#63917=SURFACE_SIDE_STYLE('',(#63916));
#63918=SURFACE_STYLE_USAGE(.BOTH.,#63917);
#63919=PRESENTATION_STYLE_ASSIGNMENT((#63918));
ENDSEC;
END-ISO-10303-21;
